ISO-10303-21;
HEADER;
/* Generated by software containing ST-Developer
 * from STEP Tools, Inc. (www.steptools.com) 
 */

FILE_DESCRIPTION(
/* description */ ('Located fixture plate with toggle clamp'),
/* implementation_level */ '2;1');

FILE_NAME(
/* name */ 'Flat Washer - M6.step',
/* time_stamp */ '2026-10-27T21:36:12-07:00',
/* author */ (''),
/* organization */ (''),
/* preprocessor_version */ 'ST-DEVELOPER v20.2',
/* originating_system */ 'Autodesk Translation Framework v15.17.0.0',
/* authorisation */ '');

FILE_SCHEMA (('AUTOMOTIVE_DESIGN { 1 0 10303 214 3 1 1 }'));
ENDSEC;

DATA;
#10=MECHANICAL_DESIGN_GEOMETRIC_PRESENTATION_REPRESENTATION('',(#342),#9285);
#294=SHAPE_REPRESENTATION_RELATIONSHIP('SRR','None',#9420,#318);
#318=ADVANCED_BREP_SHAPE_REPRESENTATION('',(#363),#9282);
#342=STYLED_ITEM('',(#9619),#363);
#363=MANIFOLD_SOLID_BREP('Body1',#5193);
#481=FACE_BOUND('',#1368,.T.);
#482=FACE_BOUND('',#1370,.T.);
#666=PLANE('',#5962);
#667=PLANE('',#5963);
#955=FACE_OUTER_BOUND('',#1365,.T.);
#956=FACE_OUTER_BOUND('',#1366,.T.);
#957=FACE_OUTER_BOUND('',#1367,.T.);
#958=FACE_OUTER_BOUND('',#1369,.T.);
#1365=EDGE_LOOP('',(#4744,#4745,#4746,#4747));
#1366=EDGE_LOOP('',(#4748,#4749,#4750,#4751));
#1367=EDGE_LOOP('',(#4752));
#1368=EDGE_LOOP('',(#4753));
#1369=EDGE_LOOP('',(#4754));
#1370=EDGE_LOOP('',(#4755));
#1568=CIRCLE('',#5957,0.32);
#1569=CIRCLE('',#5958,0.32);
#1570=CIRCLE('',#5960,0.6);
#1571=CIRCLE('',#5961,0.6);
#1982=LINE('',#9080,#2392);
#1983=LINE('',#9086,#2393);
#2392=VECTOR('',#7424,0.32);
#2393=VECTOR('',#7431,0.6);
#2814=VERTEX_POINT('',#9077);
#2815=VERTEX_POINT('',#9079);
#2816=VERTEX_POINT('',#9083);
#2817=VERTEX_POINT('',#9085);
#3460=EDGE_CURVE('',#2814,#2814,#1568,.T.);
#3461=EDGE_CURVE('',#2814,#2815,#1982,.T.);
#3462=EDGE_CURVE('',#2815,#2815,#1569,.T.);
#3463=EDGE_CURVE('',#2816,#2816,#1570,.T.);
#3464=EDGE_CURVE('',#2816,#2817,#1983,.T.);
#3465=EDGE_CURVE('',#2817,#2817,#1571,.T.);
#4744=ORIENTED_EDGE('',*,*,#3460,.F.);
#4745=ORIENTED_EDGE('',*,*,#3461,.T.);
#4746=ORIENTED_EDGE('',*,*,#3462,.T.);
#4747=ORIENTED_EDGE('',*,*,#3461,.F.);
#4748=ORIENTED_EDGE('',*,*,#3463,.F.);
#4749=ORIENTED_EDGE('',*,*,#3464,.T.);
#4750=ORIENTED_EDGE('',*,*,#3465,.T.);
#4751=ORIENTED_EDGE('',*,*,#3464,.F.);
#4752=ORIENTED_EDGE('',*,*,#3463,.T.);
#4753=ORIENTED_EDGE('',*,*,#3460,.T.);
#4754=ORIENTED_EDGE('',*,*,#3465,.F.);
#4755=ORIENTED_EDGE('',*,*,#3462,.F.);
#4869=CYLINDRICAL_SURFACE('',#5956,0.32);
#4870=CYLINDRICAL_SURFACE('',#5959,0.6);
#5156=ADVANCED_FACE('',(#955),#4869,.F.);
#5157=ADVANCED_FACE('',(#956),#4870,.T.);
#5158=ADVANCED_FACE('',(#957,#481),#666,.T.);
#5159=ADVANCED_FACE('',(#958,#482),#667,.F.);
#5193=CLOSED_SHELL('',(#5156,#5157,#5158,#5159));
#5955=AXIS2_PLACEMENT_3D('',#9075,#7418,#7419);
#5956=AXIS2_PLACEMENT_3D('',#9076,#7420,#7421);
#5957=AXIS2_PLACEMENT_3D('',#9078,#7422,#7423);
#5958=AXIS2_PLACEMENT_3D('',#9081,#7425,#7426);
#5959=AXIS2_PLACEMENT_3D('',#9082,#7427,#7428);
#5960=AXIS2_PLACEMENT_3D('',#9084,#7429,#7430);
#5961=AXIS2_PLACEMENT_3D('',#9087,#7432,#7433);
#5962=AXIS2_PLACEMENT_3D('',#9088,#7434,#7435);
#5963=AXIS2_PLACEMENT_3D('',#9089,#7436,#7437);
#7418=DIRECTION('axis',(0.,0.,1.));
#7419=DIRECTION('refdir',(1.,0.,0.));
#7420=DIRECTION('center_axis',(0.,1.,0.));
#7421=DIRECTION('ref_axis',(1.,0.,0.));
#7422=DIRECTION('center_axis',(0.,-1.,0.));
#7423=DIRECTION('ref_axis',(1.,0.,0.));
#7424=DIRECTION('',(0.,-1.,0.));
#7425=DIRECTION('center_axis',(0.,-1.,0.));
#7426=DIRECTION('ref_axis',(1.,0.,0.));
#7427=DIRECTION('center_axis',(0.,1.,0.));
#7428=DIRECTION('ref_axis',(1.,0.,0.));
#7429=DIRECTION('center_axis',(0.,1.,0.));
#7430=DIRECTION('ref_axis',(1.,0.,0.));
#7431=DIRECTION('',(0.,-1.,0.));
#7432=DIRECTION('center_axis',(0.,1.,0.));
#7433=DIRECTION('ref_axis',(1.,0.,0.));
#7434=DIRECTION('center_axis',(0.,1.,0.));
#7435=DIRECTION('ref_axis',(1.,0.,0.));
#7436=DIRECTION('center_axis',(0.,1.,0.));
#7437=DIRECTION('ref_axis',(1.,0.,0.));
#9075=CARTESIAN_POINT('',(0.,0.,0.));
#9076=CARTESIAN_POINT('Origin',(0.,0.,0.));
#9077=CARTESIAN_POINT('',(-0.32,0.16,3.91886975727153E-17));
#9078=CARTESIAN_POINT('Origin',(0.,0.16,0.));
#9079=CARTESIAN_POINT('',(-0.32,0.,3.91886975727153E-17));
#9080=CARTESIAN_POINT('',(-0.32,0.,3.91886975727153E-17));
#9081=CARTESIAN_POINT('Origin',(0.,0.,0.));
#9082=CARTESIAN_POINT('Origin',(0.,0.,0.));
#9083=CARTESIAN_POINT('',(-0.6,0.16,7.34788079488412E-17));
#9084=CARTESIAN_POINT('Origin',(0.,0.16,0.));
#9085=CARTESIAN_POINT('',(-0.6,0.,7.34788079488412E-17));
#9086=CARTESIAN_POINT('',(-0.6,0.,7.34788079488412E-17));
#9087=CARTESIAN_POINT('Origin',(0.,0.,0.));
#9088=CARTESIAN_POINT('Origin',(0.,0.16,0.));
#9089=CARTESIAN_POINT('Origin',(0.,0.,0.));
#9252=UNCERTAINTY_MEASURE_WITH_UNIT(LENGTH_MEASURE(0.001),#9286,
'DISTANCE_ACCURACY_VALUE',
'Maximum model space distance between geometric entities at asserted c
onnectivities');
#9255=UNCERTAINTY_MEASURE_WITH_UNIT(LENGTH_MEASURE(0.001),#9286,
'DISTANCE_ACCURACY_VALUE',
'Maximum model space distance between geometric entities at asserted c
onnectivities');
#9282=(
GEOMETRIC_REPRESENTATION_CONTEXT(3)
GLOBAL_UNCERTAINTY_ASSIGNED_CONTEXT((#9252))
GLOBAL_UNIT_ASSIGNED_CONTEXT((#9286,#9288,#9289))
REPRESENTATION_CONTEXT('','3D')
);
#9285=(
GEOMETRIC_REPRESENTATION_CONTEXT(3)
GLOBAL_UNCERTAINTY_ASSIGNED_CONTEXT((#9255))
GLOBAL_UNIT_ASSIGNED_CONTEXT((#9286,#9288,#9289))
REPRESENTATION_CONTEXT('','3D')
);
#9286=(
LENGTH_UNIT()
NAMED_UNIT(*)
SI_UNIT(.CENTI.,.METRE.)
);
#9288=(
NAMED_UNIT(*)
PLANE_ANGLE_UNIT()
SI_UNIT($,.RADIAN.)
);
#9289=(
NAMED_UNIT(*)
SI_UNIT($,.STERADIAN.)
SOLID_ANGLE_UNIT()
);
#9316=SHAPE_DEFINITION_REPRESENTATION(#9346,#9420);
#9346=PRODUCT_DEFINITION_SHAPE('',$,#9450);
#9420=SHAPE_REPRESENTATION('',(#5955),#9282);
#9423=PRODUCT_DEFINITION_CONTEXT('part definition',#9512,'design');
#9450=PRODUCT_DEFINITION('Flat Washer - M6','Flat Washer - M6',#9479,#9423);
#9479=PRODUCT_DEFINITION_FORMATION('',$,#9540);
#9512=APPLICATION_CONTEXT(
'Core Data for Automotive Mechanical Design Process');
#9513=PRODUCT_CONTEXT('part definition',#9512,'mechanical');
#9540=PRODUCT('Flat Washer - M6','Flat Washer - M6','Flat Washer - M6',
(#9513));
#9613=COLOUR_RGB('Black',0.12,0.14,0.17);
#9614=FILL_AREA_STYLE_COLOUR('',#9613);
#9615=FILL_AREA_STYLE('',(#9614));
#9616=SURFACE_STYLE_FILL_AREA(#9615);
#9617=SURFACE_SIDE_STYLE('',(#9616));
#9618=SURFACE_STYLE_USAGE(.BOTH.,#9617);
#9619=PRESENTATION_STYLE_ASSIGNMENT((#9618));
ENDSEC;
END-ISO-10303-21;
